ISO-10303-21;
HEADER;
/* Generated by software containing ST-Developer
 * from STEP Tools, Inc. (www.steptools.com) 
 */

FILE_DESCRIPTION(
/* description */ ('Four-valve pipe header'),
/* implementation_level */ '2;1');

FILE_NAME(
/* name */ 'Hex Bolt - M6 x 30 mm.step',
/* time_stamp */ '2026-10-29T16:56:19-07:00',
/* author */ (''),
/* organization */ (''),
/* preprocessor_version */ 'ST-DEVELOPER v20.2',
/* originating_system */ 'Autodesk Translation Framework v15.17.0.0',
/* authorisation */ '');

FILE_SCHEMA (('AUTOMOTIVE_DESIGN { 1 0 10303 214 3 1 1 }'));
ENDSEC;

DATA;
#10=MECHANICAL_DESIGN_GEOMETRIC_PRESENTATION_REPRESENTATION('',(#337),#10119);
#246=(
BOUNDED_CURVE()
B_SPLINE_CURVE(2,(#8906,#8907,#8908),.UNSPECIFIED.,.F.,.F.)
B_SPLINE_CURVE_WITH_KNOTS((3,3),(0.144988513094728,0.791574906712449),
 .UNSPECIFIED.)
CURVE()
GEOMETRIC_REPRESENTATION_ITEM()
RATIONAL_B_SPLINE_CURVE((1.09282032302755,1.26188021535082,1.09282032302931))
REPRESENTATION_ITEM('')
);
#247=(
BOUNDED_CURVE()
B_SPLINE_CURVE(2,(#8910,#8911,#8912),.UNSPECIFIED.,.F.,.F.)
B_SPLINE_CURVE_WITH_KNOTS((3,3),(0.144988513094728,0.791574906712449),
 .UNSPECIFIED.)
CURVE()
GEOMETRIC_REPRESENTATION_ITEM()
RATIONAL_B_SPLINE_CURVE((1.09282032302755,1.26188021535082,1.09282032302931))
REPRESENTATION_ITEM('')
);
#248=(
BOUNDED_CURVE()
B_SPLINE_CURVE(2,(#8914,#8915,#8916),.UNSPECIFIED.,.F.,.F.)
B_SPLINE_CURVE_WITH_KNOTS((3,3),(0.144988513094728,0.791574906712449),
 .UNSPECIFIED.)
CURVE()
GEOMETRIC_REPRESENTATION_ITEM()
RATIONAL_B_SPLINE_CURVE((1.09282032302755,1.26188021535082,1.09282032302931))
REPRESENTATION_ITEM('')
);
#249=(
BOUNDED_CURVE()
B_SPLINE_CURVE(2,(#8918,#8919,#8920),.UNSPECIFIED.,.F.,.F.)
B_SPLINE_CURVE_WITH_KNOTS((3,3),(0.144988513094728,0.791574906712449),
 .UNSPECIFIED.)
CURVE()
GEOMETRIC_REPRESENTATION_ITEM()
RATIONAL_B_SPLINE_CURVE((1.09282032302755,1.26188021535082,1.09282032302931))
REPRESENTATION_ITEM('')
);
#250=(
BOUNDED_CURVE()
B_SPLINE_CURVE(2,(#8922,#8923,#8924),.UNSPECIFIED.,.F.,.F.)
B_SPLINE_CURVE_WITH_KNOTS((3,3),(0.144988513094728,0.791574906712449),
 .UNSPECIFIED.)
CURVE()
GEOMETRIC_REPRESENTATION_ITEM()
RATIONAL_B_SPLINE_CURVE((1.09282032302755,1.26188021535082,1.09282032302931))
REPRESENTATION_ITEM('')
);
#251=(
BOUNDED_CURVE()
B_SPLINE_CURVE(2,(#8925,#8926,#8927),.UNSPECIFIED.,.F.,.F.)
B_SPLINE_CURVE_WITH_KNOTS((3,3),(0.144988513094727,0.791574906712449),
 .UNSPECIFIED.)
CURVE()
GEOMETRIC_REPRESENTATION_ITEM()
RATIONAL_B_SPLINE_CURVE((1.09282032302755,1.26188021535082,1.09282032302931))
REPRESENTATION_ITEM('')
);
#264=CONICAL_SURFACE('',#6092,0.27,0.785398163397448);
#265=CONICAL_SURFACE('',#6095,0.576175134594813,1.0471975511966);
#285=SHAPE_REPRESENTATION_RELATIONSHIP('SRR','None',#10246,#311);
#311=ADVANCED_BREP_SHAPE_REPRESENTATION('',(#363),#10095);
#337=STYLED_ITEM('',(#10477),#363);
#363=MANIFOLD_SOLID_BREP('Body1',#5583);
#455=FACE_BOUND('',#1211,.T.);
#588=PLANE('',#6094);
#589=PLANE('',#6097);
#590=PLANE('',#6098);
#591=PLANE('',#6099);
#592=PLANE('',#6100);
#593=PLANE('',#6101);
#594=PLANE('',#6102);
#595=PLANE('',#6103);
#596=PLANE('',#6104);
#838=FACE_OUTER_BOUND('',#1199,.T.);
#839=FACE_OUTER_BOUND('',#1200,.T.);
#840=FACE_OUTER_BOUND('',#1201,.T.);
#841=FACE_OUTER_BOUND('',#1202,.T.);
#842=FACE_OUTER_BOUND('',#1203,.T.);
#843=FACE_OUTER_BOUND('',#1204,.T.);
#844=FACE_OUTER_BOUND('',#1205,.T.);
#845=FACE_OUTER_BOUND('',#1206,.T.);
#846=FACE_OUTER_BOUND('',#1207,.T.);
#847=FACE_OUTER_BOUND('',#1208,.T.);
#848=FACE_OUTER_BOUND('',#1209,.T.);
#849=FACE_OUTER_BOUND('',#1210,.T.);
#1199=EDGE_LOOP('',(#4165,#4166,#4167,#4168));
#1200=EDGE_LOOP('',(#4169,#4170,#4171,#4172));
#1201=EDGE_LOOP('',(#4173));
#1202=EDGE_LOOP('',(#4174,#4175,#4176,#4177,#4178,#4179,#4180,#4181,#4182));
#1203=EDGE_LOOP('',(#4183,#4184,#4185,#4186));
#1204=EDGE_LOOP('',(#4187,#4188,#4189,#4190));
#1205=EDGE_LOOP('',(#4191,#4192,#4193,#4194));
#1206=EDGE_LOOP('',(#4195,#4196,#4197,#4198));
#1207=EDGE_LOOP('',(#4199,#4200,#4201,#4202));
#1208=EDGE_LOOP('',(#4203,#4204,#4205,#4206));
#1209=EDGE_LOOP('',(#4207));
#1210=EDGE_LOOP('',(#4208,#4209,#4210,#4211,#4212,#4213));
#1211=EDGE_LOOP('',(#4214));
#1624=LINE('',#8893,#2042);
#1625=LINE('',#8898,#2043);
#1626=LINE('',#8904,#2044);
#1627=LINE('',#8930,#2045);
#1628=LINE('',#8932,#2046);
#1629=LINE('',#8933,#2047);
#1630=LINE('',#8936,#2048);
#1631=LINE('',#8937,#2049);
#1632=LINE('',#8940,#2050);
#1633=LINE('',#8941,#2051);
#1634=LINE('',#8944,#2052);
#1635=LINE('',#8945,#2053);
#1636=LINE('',#8948,#2054);
#1637=LINE('',#8949,#2055);
#1638=LINE('',#8951,#2056);
#2042=VECTOR('',#7065,0.3);
#2043=VECTOR('',#7072,0.27);
#2044=VECTOR('',#7079,0.576175134594813);
#2045=VECTOR('',#7082,1.);
#2046=VECTOR('',#7083,1.);
#2047=VECTOR('',#7084,1.);
#2048=VECTOR('',#7087,1.);
#2049=VECTOR('',#7088,1.);
#2050=VECTOR('',#7091,1.);
#2051=VECTOR('',#7092,1.);
#2052=VECTOR('',#7095,1.);
#2053=VECTOR('',#7096,1.);
#2054=VECTOR('',#7099,1.);
#2055=VECTOR('',#7100,1.);
#2056=VECTOR('',#7103,1.);
#2420=CIRCLE('',#6090,0.2942);
#2421=CIRCLE('',#6091,0.2942);
#2422=CIRCLE('',#6093,0.24);
#2423=CIRCLE('',#6096,0.475);
#2716=VERTEX_POINT('',#8890);
#2717=VERTEX_POINT('',#8892);
#2718=VERTEX_POINT('',#8896);
#2719=VERTEX_POINT('',#8901);
#2720=VERTEX_POINT('',#8903);
#2721=VERTEX_POINT('',#8905);
#2722=VERTEX_POINT('',#8909);
#2723=VERTEX_POINT('',#8913);
#2724=VERTEX_POINT('',#8917);
#2725=VERTEX_POINT('',#8921);
#2726=VERTEX_POINT('',#8929);
#2727=VERTEX_POINT('',#8931);
#2728=VERTEX_POINT('',#8935);
#2729=VERTEX_POINT('',#8939);
#2730=VERTEX_POINT('',#8943);
#2731=VERTEX_POINT('',#8947);
#3249=EDGE_CURVE('',#2716,#2716,#2420,.F.);
#3250=EDGE_CURVE('',#2716,#2717,#1624,.T.);
#3251=EDGE_CURVE('',#2717,#2717,#2421,.F.);
#3252=EDGE_CURVE('',#2718,#2718,#2422,.T.);
#3253=EDGE_CURVE('',#2718,#2716,#1625,.T.);
#3254=EDGE_CURVE('',#2719,#2719,#2423,.T.);
#3255=EDGE_CURVE('',#2719,#2720,#1626,.T.);
#3256=EDGE_CURVE('',#2721,#2720,#246,.T.);
#3257=EDGE_CURVE('',#2722,#2721,#247,.T.);
#3258=EDGE_CURVE('',#2723,#2722,#248,.T.);
#3259=EDGE_CURVE('',#2724,#2723,#249,.T.);
#3260=EDGE_CURVE('',#2725,#2724,#250,.T.);
#3261=EDGE_CURVE('',#2720,#2725,#251,.T.);
#3262=EDGE_CURVE('',#2726,#2724,#1627,.T.);
#3263=EDGE_CURVE('',#2726,#2727,#1628,.T.);
#3264=EDGE_CURVE('',#2727,#2725,#1629,.T.);
#3265=EDGE_CURVE('',#2728,#2723,#1630,.T.);
#3266=EDGE_CURVE('',#2728,#2726,#1631,.T.);
#3267=EDGE_CURVE('',#2729,#2722,#1632,.T.);
#3268=EDGE_CURVE('',#2729,#2728,#1633,.T.);
#3269=EDGE_CURVE('',#2730,#2721,#1634,.T.);
#3270=EDGE_CURVE('',#2730,#2729,#1635,.T.);
#3271=EDGE_CURVE('',#2731,#2720,#1636,.T.);
#3272=EDGE_CURVE('',#2731,#2730,#1637,.T.);
#3273=EDGE_CURVE('',#2727,#2731,#1638,.T.);
#4165=ORIENTED_EDGE('',*,*,#3249,.F.);
#4166=ORIENTED_EDGE('',*,*,#3250,.T.);
#4167=ORIENTED_EDGE('',*,*,#3251,.F.);
#4168=ORIENTED_EDGE('',*,*,#3250,.F.);
#4169=ORIENTED_EDGE('',*,*,#3252,.F.);
#4170=ORIENTED_EDGE('',*,*,#3253,.T.);
#4171=ORIENTED_EDGE('',*,*,#3249,.T.);
#4172=ORIENTED_EDGE('',*,*,#3253,.F.);
#4173=ORIENTED_EDGE('',*,*,#3252,.T.);
#4174=ORIENTED_EDGE('',*,*,#3254,.F.);
#4175=ORIENTED_EDGE('',*,*,#3255,.T.);
#4176=ORIENTED_EDGE('',*,*,#3256,.F.);
#4177=ORIENTED_EDGE('',*,*,#3257,.F.);
#4178=ORIENTED_EDGE('',*,*,#3258,.F.);
#4179=ORIENTED_EDGE('',*,*,#3259,.F.);
#4180=ORIENTED_EDGE('',*,*,#3260,.F.);
#4181=ORIENTED_EDGE('',*,*,#3261,.F.);
#4182=ORIENTED_EDGE('',*,*,#3255,.F.);
#4183=ORIENTED_EDGE('',*,*,#3260,.T.);
#4184=ORIENTED_EDGE('',*,*,#3262,.F.);
#4185=ORIENTED_EDGE('',*,*,#3263,.T.);
#4186=ORIENTED_EDGE('',*,*,#3264,.T.);
#4187=ORIENTED_EDGE('',*,*,#3259,.T.);
#4188=ORIENTED_EDGE('',*,*,#3265,.F.);
#4189=ORIENTED_EDGE('',*,*,#3266,.T.);
#4190=ORIENTED_EDGE('',*,*,#3262,.T.);
#4191=ORIENTED_EDGE('',*,*,#3258,.T.);
#4192=ORIENTED_EDGE('',*,*,#3267,.F.);
#4193=ORIENTED_EDGE('',*,*,#3268,.T.);
#4194=ORIENTED_EDGE('',*,*,#3265,.T.);
#4195=ORIENTED_EDGE('',*,*,#3257,.T.);
#4196=ORIENTED_EDGE('',*,*,#3269,.F.);
#4197=ORIENTED_EDGE('',*,*,#3270,.T.);
#4198=ORIENTED_EDGE('',*,*,#3267,.T.);
#4199=ORIENTED_EDGE('',*,*,#3256,.T.);
#4200=ORIENTED_EDGE('',*,*,#3271,.F.);
#4201=ORIENTED_EDGE('',*,*,#3272,.T.);
#4202=ORIENTED_EDGE('',*,*,#3269,.T.);
#4203=ORIENTED_EDGE('',*,*,#3261,.T.);
#4204=ORIENTED_EDGE('',*,*,#3264,.F.);
#4205=ORIENTED_EDGE('',*,*,#3273,.T.);
#4206=ORIENTED_EDGE('',*,*,#3271,.T.);
#4207=ORIENTED_EDGE('',*,*,#3254,.T.);
#4208=ORIENTED_EDGE('',*,*,#3268,.F.);
#4209=ORIENTED_EDGE('',*,*,#3270,.F.);
#4210=ORIENTED_EDGE('',*,*,#3272,.F.);
#4211=ORIENTED_EDGE('',*,*,#3273,.F.);
#4212=ORIENTED_EDGE('',*,*,#3263,.F.);
#4213=ORIENTED_EDGE('',*,*,#3266,.F.);
#4214=ORIENTED_EDGE('',*,*,#3251,.T.);
#5187=CYLINDRICAL_SURFACE('',#6089,0.2942);
#5338=ADVANCED_FACE('',(#838),#5187,.T.);
#5339=ADVANCED_FACE('',(#839),#264,.T.);
#5340=ADVANCED_FACE('',(#840),#588,.T.);
#5341=ADVANCED_FACE('',(#841),#265,.T.);
#5342=ADVANCED_FACE('',(#842),#589,.T.);
#5343=ADVANCED_FACE('',(#843),#590,.T.);
#5344=ADVANCED_FACE('',(#844),#591,.T.);
#5345=ADVANCED_FACE('',(#845),#592,.T.);
#5346=ADVANCED_FACE('',(#846),#593,.T.);
#5347=ADVANCED_FACE('',(#847),#594,.T.);
#5348=ADVANCED_FACE('',(#848),#595,.T.);
#5349=ADVANCED_FACE('',(#849,#455),#596,.F.);
#5583=CLOSED_SHELL('',(#5338,#5339,#5340,#5341,#5342,#5343,#5344,#5345,
#5346,#5347,#5348,#5349));
#6088=AXIS2_PLACEMENT_3D('',#8888,#7059,#7060);
#6089=AXIS2_PLACEMENT_3D('',#8889,#7061,#7062);
#6090=AXIS2_PLACEMENT_3D('',#8891,#7063,#7064);
#6091=AXIS2_PLACEMENT_3D('',#8894,#7066,#7067);
#6092=AXIS2_PLACEMENT_3D('',#8895,#7068,#7069);
#6093=AXIS2_PLACEMENT_3D('',#8897,#7070,#7071);
#6094=AXIS2_PLACEMENT_3D('',#8899,#7073,#7074);
#6095=AXIS2_PLACEMENT_3D('',#8900,#7075,#7076);
#6096=AXIS2_PLACEMENT_3D('',#8902,#7077,#7078);
#6097=AXIS2_PLACEMENT_3D('',#8928,#7080,#7081);
#6098=AXIS2_PLACEMENT_3D('',#8934,#7085,#7086);
#6099=AXIS2_PLACEMENT_3D('',#8938,#7089,#7090);
#6100=AXIS2_PLACEMENT_3D('',#8942,#7093,#7094);
#6101=AXIS2_PLACEMENT_3D('',#8946,#7097,#7098);
#6102=AXIS2_PLACEMENT_3D('',#8950,#7101,#7102);
#6103=AXIS2_PLACEMENT_3D('',#8952,#7104,#7105);
#6104=AXIS2_PLACEMENT_3D('',#8953,#7106,#7107);
#7059=DIRECTION('axis',(0.,0.,1.));
#7060=DIRECTION('refdir',(1.,0.,0.));
#7061=DIRECTION('center_axis',(0.,-1.,0.));
#7062=DIRECTION('ref_axis',(1.,0.,0.));
#7063=DIRECTION('center_axis',(0.,1.,0.));
#7064=DIRECTION('ref_axis',(1.,0.,0.));
#7065=DIRECTION('',(0.,1.,0.));
#7066=DIRECTION('center_axis',(0.,-1.,0.));
#7067=DIRECTION('ref_axis',(1.,0.,0.));
#7068=DIRECTION('center_axis',(0.,1.,0.));
#7069=DIRECTION('ref_axis',(1.,0.,0.));
#7070=DIRECTION('center_axis',(0.,-1.,0.));
#7071=DIRECTION('ref_axis',(1.,0.,0.));
#7072=DIRECTION('',(-0.707106781186547,0.707106781186548,-8.65956056235493E-17));
#7073=DIRECTION('center_axis',(0.,-1.,0.));
#7074=DIRECTION('ref_axis',(0.,0.,-1.));
#7075=DIRECTION('center_axis',(0.,-1.,0.));
#7076=DIRECTION('ref_axis',(1.,0.,0.));
#7077=DIRECTION('center_axis',(0.,1.,0.));
#7078=DIRECTION('ref_axis',(1.,0.,0.));
#7079=DIRECTION('',(-0.866025403784439,-0.5,-1.06057523872491E-16));
#7080=DIRECTION('center_axis',(1.92296268638356E-16,0.,-1.));
#7081=DIRECTION('ref_axis',(-1.,0.,-1.92296268638356E-16));
#7082=DIRECTION('',(0.,1.,0.));
#7083=DIRECTION('',(-1.,0.,-1.92296268638356E-16));
#7084=DIRECTION('',(0.,1.,0.));
#7085=DIRECTION('center_axis',(0.866025403784439,0.,-0.5));
#7086=DIRECTION('ref_axis',(-0.5,0.,-0.866025403784439));
#7087=DIRECTION('',(0.,1.,0.));
#7088=DIRECTION('',(-0.5,0.,-0.866025403784439));
#7089=DIRECTION('center_axis',(0.866025403784439,0.,0.5));
#7090=DIRECTION('ref_axis',(0.5,0.,-0.866025403784439));
#7091=DIRECTION('',(0.,1.,0.));
#7092=DIRECTION('',(0.5,0.,-0.866025403784439));
#7093=DIRECTION('center_axis',(-1.92296268638356E-16,0.,1.));
#7094=DIRECTION('ref_axis',(1.,0.,1.92296268638356E-16));
#7095=DIRECTION('',(0.,1.,0.));
#7096=DIRECTION('',(1.,0.,1.92296268638356E-16));
#7097=DIRECTION('center_axis',(-0.866025403784439,0.,0.5));
#7098=DIRECTION('ref_axis',(0.5,0.,0.866025403784439));
#7099=DIRECTION('',(0.,1.,0.));
#7100=DIRECTION('',(0.5,0.,0.866025403784439));
#7101=DIRECTION('center_axis',(-0.866025403784439,0.,-0.5));
#7102=DIRECTION('ref_axis',(-0.5,0.,0.866025403784439));
#7103=DIRECTION('',(-0.5,0.,0.866025403784438));
#7104=DIRECTION('center_axis',(0.,1.,0.));
#7105=DIRECTION('ref_axis',(0.,0.,1.));
#7106=DIRECTION('center_axis',(0.,1.,0.));
#7107=DIRECTION('ref_axis',(1.,0.,0.));
#8888=CARTESIAN_POINT('',(0.,0.,0.));
#8889=CARTESIAN_POINT('Origin',(0.,-1.445,0.));
#8890=CARTESIAN_POINT('',(-0.2942,-2.9458,3.60291088309151E-17));
#8891=CARTESIAN_POINT('Origin',(0.,-2.9458,0.));
#8892=CARTESIAN_POINT('',(-0.2942,0.,-3.60291088309151E-17));
#8893=CARTESIAN_POINT('',(-0.2942,-1.445,-3.60291088309151E-17));
#8894=CARTESIAN_POINT('Origin',(0.,0.,0.));
#8895=CARTESIAN_POINT('Origin',(0.,-2.97,0.));
#8896=CARTESIAN_POINT('',(-0.24,-3.,-2.93915231795365E-17));
#8897=CARTESIAN_POINT('Origin',(0.,-3.,0.));
#8898=CARTESIAN_POINT('',(-0.27,-2.97,-3.30654635769785E-17));
#8899=CARTESIAN_POINT('Origin',(0.,-3.,0.));
#8900=CARTESIAN_POINT('Origin',(0.,0.341586508806388,0.));
#8901=CARTESIAN_POINT('',(-0.475,0.4,-5.81707229594993E-17));
#8902=CARTESIAN_POINT('Origin',(0.,0.4,0.));
#8903=CARTESIAN_POINT('',(-0.577350269189626,0.340908044531739,-7.07050159149938E-17));
#8904=CARTESIAN_POINT('',(-0.576175134594813,0.341586508806388,-7.05611034329833E-17));
#8905=CARTESIAN_POINT('',(-0.288675134594813,0.340908044531739,0.5));
#8906=CARTESIAN_POINT('Ctrl Pts',(-0.288675134594813,0.340908044531739,
0.5));
#8907=CARTESIAN_POINT('Ctrl Pts',(-0.433012701893303,0.424241377863696,
0.249999999998124));
#8908=CARTESIAN_POINT('Ctrl Pts',(-0.577350269189626,0.340908044531739,
-7.07050159149938E-17));
#8909=CARTESIAN_POINT('',(0.288675134594813,0.340908044531739,0.5));
#8910=CARTESIAN_POINT('Ctrl Pts',(0.288675134594813,0.340908044531739,0.5));
#8911=CARTESIAN_POINT('Ctrl Pts',(-2.16648921025353E-12,0.424241377863696,
0.5));
#8912=CARTESIAN_POINT('Ctrl Pts',(-0.288675134594813,0.340908044531739,
0.5));
#8913=CARTESIAN_POINT('',(0.577350269189626,0.340908044531739,0.));
#8914=CARTESIAN_POINT('Ctrl Pts',(0.577350269189626,0.340908044531739,0.));
#8915=CARTESIAN_POINT('Ctrl Pts',(0.433012701891136,0.424241377863697,0.250000000001876));
#8916=CARTESIAN_POINT('Ctrl Pts',(0.288675134594813,0.340908044531739,0.5));
#8917=CARTESIAN_POINT('',(0.288675134594813,0.340908044531739,-0.5));
#8918=CARTESIAN_POINT('Ctrl Pts',(0.288675134594813,0.340908044531739,-0.5));
#8919=CARTESIAN_POINT('Ctrl Pts',(0.433012701893303,0.424241377863696,-0.249999999998124));
#8920=CARTESIAN_POINT('Ctrl Pts',(0.577350269189626,0.340908044531739,0.));
#8921=CARTESIAN_POINT('',(-0.288675134594813,0.340908044531739,-0.5));
#8922=CARTESIAN_POINT('Ctrl Pts',(-0.288675134594813,0.340908044531739,
-0.5));
#8923=CARTESIAN_POINT('Ctrl Pts',(2.16660023255599E-12,0.424241377863696,
-0.5));
#8924=CARTESIAN_POINT('Ctrl Pts',(0.288675134594813,0.340908044531739,-0.5));
#8925=CARTESIAN_POINT('Ctrl Pts',(-0.577350269189626,0.340908044531739,
-7.07050159149938E-17));
#8926=CARTESIAN_POINT('Ctrl Pts',(-0.433012701891136,0.424241377863697,
-0.250000000001876));
#8927=CARTESIAN_POINT('Ctrl Pts',(-0.288675134594813,0.340908044531739,
-0.5));
#8928=CARTESIAN_POINT('Origin',(0.288675134594813,0.,-0.5));
#8929=CARTESIAN_POINT('',(0.288675134594813,0.,-0.5));
#8930=CARTESIAN_POINT('',(0.288675134594813,0.,-0.5));
#8931=CARTESIAN_POINT('',(-0.288675134594813,0.,-0.5));
#8932=CARTESIAN_POINT('',(0.288675134594813,0.,-0.5));
#8933=CARTESIAN_POINT('',(-0.288675134594813,0.,-0.5));
#8934=CARTESIAN_POINT('Origin',(0.577350269189626,0.,0.));
#8935=CARTESIAN_POINT('',(0.577350269189626,0.,0.));
#8936=CARTESIAN_POINT('',(0.577350269189626,0.,0.));
#8937=CARTESIAN_POINT('',(0.577350269189626,0.,0.));
#8938=CARTESIAN_POINT('Origin',(0.288675134594813,0.,0.5));
#8939=CARTESIAN_POINT('',(0.288675134594813,0.,0.5));
#8940=CARTESIAN_POINT('',(0.288675134594813,0.,0.5));
#8941=CARTESIAN_POINT('',(0.288675134594813,0.,0.5));
#8942=CARTESIAN_POINT('Origin',(-0.288675134594813,0.,0.5));
#8943=CARTESIAN_POINT('',(-0.288675134594813,0.,0.5));
#8944=CARTESIAN_POINT('',(-0.288675134594813,0.,0.5));
#8945=CARTESIAN_POINT('',(-0.288675134594813,0.,0.5));
#8946=CARTESIAN_POINT('Origin',(-0.577350269189626,0.,-7.07050159149938E-17));
#8947=CARTESIAN_POINT('',(-0.577350269189626,0.,-7.07050159149938E-17));
#8948=CARTESIAN_POINT('',(-0.577350269189626,0.,-7.07050159149938E-17));
#8949=CARTESIAN_POINT('',(-0.577350269189626,0.,-7.07050159149938E-17));
#8950=CARTESIAN_POINT('Origin',(-0.288675134594813,0.,-0.5));
#8951=CARTESIAN_POINT('',(-0.288675134594813,0.,-0.5));
#8952=CARTESIAN_POINT('Origin',(0.,0.4,0.));
#8953=CARTESIAN_POINT('Origin',(0.,0.,0.));
#10064=UNCERTAINTY_MEASURE_WITH_UNIT(LENGTH_MEASURE(0.001),#10120,
'DISTANCE_ACCURACY_VALUE',
'Maximum model space distance between geometric entities at asserted c
onnectivities');
#10088=UNCERTAINTY_MEASURE_WITH_UNIT(LENGTH_MEASURE(0.001),#10120,
'DISTANCE_ACCURACY_VALUE',
'Maximum model space distance between geometric entities at asserted c
onnectivities');
#10095=(
GEOMETRIC_REPRESENTATION_CONTEXT(3)
GLOBAL_UNCERTAINTY_ASSIGNED_CONTEXT((#10064))
GLOBAL_UNIT_ASSIGNED_CONTEXT((#10120,#10122,#10123))
REPRESENTATION_CONTEXT('','3D')
);
#10119=(
GEOMETRIC_REPRESENTATION_CONTEXT(3)
GLOBAL_UNCERTAINTY_ASSIGNED_CONTEXT((#10088))
GLOBAL_UNIT_ASSIGNED_CONTEXT((#10120,#10122,#10123))
REPRESENTATION_CONTEXT('','3D')
);
#10120=(
LENGTH_UNIT()
NAMED_UNIT(*)
SI_UNIT(.CENTI.,.METRE.)
);
#10122=(
NAMED_UNIT(*)
PLANE_ANGLE_UNIT()
SI_UNIT($,.RADIAN.)
);
#10123=(
NAMED_UNIT(*)
SI_UNIT($,.STERADIAN.)
SOLID_ANGLE_UNIT()
);
#10130=SHAPE_DEFINITION_REPRESENTATION(#10160,#10246);
#10160=PRODUCT_DEFINITION_SHAPE('',$,#10277);
#10246=SHAPE_REPRESENTATION('',(#6088),#10095);
#10270=PRODUCT_DEFINITION_CONTEXT('part definition',#10362,'design');
#10277=PRODUCT_DEFINITION('Hex Bolt - M6 x 30 mm',
'Hex Bolt - M6 x 30 mm',#10307,#10270);
#10307=PRODUCT_DEFINITION_FORMATION('',$,#10370);
#10362=APPLICATION_CONTEXT(
'Core Data for Automotive Mechanical Design Process');
#10363=PRODUCT_CONTEXT('part definition',#10362,'mechanical');
#10370=PRODUCT('Hex Bolt - M6 x 30 mm','Hex Bolt - M6 x 30 mm',
'Hex Bolt - M6 x 30 mm',(#10363));
#10471=COLOUR_RGB('Black',0.12,0.14,0.17);
#10472=FILL_AREA_STYLE_COLOUR('',#10471);
#10473=FILL_AREA_STYLE('',(#10472));
#10474=SURFACE_STYLE_FILL_AREA(#10473);
#10475=SURFACE_SIDE_STYLE('',(#10474));
#10476=SURFACE_STYLE_USAGE(.BOTH.,#10475);
#10477=PRESENTATION_STYLE_ASSIGNMENT((#10476));
ENDSEC;
END-ISO-10303-21;
